ISO-10303-21;
HEADER;
/* Generated by software containing ST-Developer
 * from STEP Tools, Inc. (www.steptools.com) 
 */

FILE_DESCRIPTION(
/* description */ ('PAT-091'),
/* implementation_level */ '2;1');

FILE_NAME(
/* name */ 'Rising arm (1).step',
/* time_stamp */ '2026-10-27T15:34:44-07:00',
/* author */ (''),
/* organization */ (''),
/* preprocessor_version */ 'ST-DEVELOPER v20.2',
/* originating_system */ 'Autodesk Translation Framework v15.17.0.0',
/* authorisation */ '');

FILE_SCHEMA (('AUTOMOTIVE_DESIGN { 1 0 10303 214 3 1 1 }'));
ENDSEC;

DATA;
#10=MECHANICAL_DESIGN_GEOMETRIC_PRESENTATION_REPRESENTATION('',(#1031),#25100);
#811=SHAPE_REPRESENTATION_RELATIONSHIP('SRR','None',#25577,#921);
#921=ADVANCED_BREP_SHAPE_REPRESENTATION('',(#1153),#25047);
#1031=STYLED_ITEM('',(#26177),#1153);
#1153=MANIFOLD_SOLID_BREP('Body1',#13310);
#1496=FACE_BOUND('',#3644,.T.);
#1497=FACE_BOUND('',#3645,.T.);
#1498=FACE_BOUND('',#3646,.T.);
#1499=FACE_BOUND('',#3651,.T.);
#1500=FACE_BOUND('',#3652,.T.);
#1501=FACE_BOUND('',#3653,.T.);
#1907=PLANE('',#15551);
#1908=PLANE('',#15552);
#1909=PLANE('',#15553);
#1910=PLANE('',#15560);
#1911=PLANE('',#15563);
#1912=PLANE('',#15568);
#2536=FACE_OUTER_BOUND('',#3635,.T.);
#2537=FACE_OUTER_BOUND('',#3636,.T.);
#2538=FACE_OUTER_BOUND('',#3637,.T.);
#2539=FACE_OUTER_BOUND('',#3638,.T.);
#2540=FACE_OUTER_BOUND('',#3639,.T.);
#2541=FACE_OUTER_BOUND('',#3640,.T.);
#2542=FACE_OUTER_BOUND('',#3641,.T.);
#2543=FACE_OUTER_BOUND('',#3642,.T.);
#2544=FACE_OUTER_BOUND('',#3643,.T.);
#2545=FACE_OUTER_BOUND('',#3647,.T.);
#2546=FACE_OUTER_BOUND('',#3648,.T.);
#2547=FACE_OUTER_BOUND('',#3649,.T.);
#2548=FACE_OUTER_BOUND('',#3650,.T.);
#3635=EDGE_LOOP('',(#10876,#10877,#10878,#10879));
#3636=EDGE_LOOP('',(#10880,#10881,#10882,#10883));
#3637=EDGE_LOOP('',(#10884,#10885,#10886,#10887));
#3638=EDGE_LOOP('',(#10888,#10889,#10890,#10891));
#3639=EDGE_LOOP('',(#10892,#10893,#10894,#10895));
#3640=EDGE_LOOP('',(#10896,#10897,#10898,#10899));
#3641=EDGE_LOOP('',(#10900,#10901,#10902,#10903));
#3642=EDGE_LOOP('',(#10904,#10905,#10906,#10907));
#3643=EDGE_LOOP('',(#10908,#10909,#10910,#10911,#10912,#10913,#10914,#10915));
#3644=EDGE_LOOP('',(#10916));
#3645=EDGE_LOOP('',(#10917));
#3646=EDGE_LOOP('',(#10918));
#3647=EDGE_LOOP('',(#10919,#10920,#10921,#10922));
#3648=EDGE_LOOP('',(#10923,#10924,#10925,#10926));
#3649=EDGE_LOOP('',(#10927,#10928,#10929,#10930));
#3650=EDGE_LOOP('',(#10931,#10932,#10933,#10934,#10935,#10936,#10937,#10938));
#3651=EDGE_LOOP('',(#10939));
#3652=EDGE_LOOP('',(#10940));
#3653=EDGE_LOOP('',(#10941));
#4658=LINE('',#23157,#5398);
#4659=LINE('',#23162,#5399);
#4660=LINE('',#23166,#5400);
#4661=LINE('',#23171,#5401);
#4662=LINE('',#23175,#5402);
#4663=LINE('',#23179,#5403);
#4664=LINE('',#23181,#5404);
#4665=LINE('',#23182,#5405);
#4666=LINE('',#23185,#5406);
#4667=LINE('',#23187,#5407);
#4668=LINE('',#23188,#5408);
#4669=LINE('',#23191,#5409);
#4670=LINE('',#23193,#5410);
#4671=LINE('',#23194,#5411);
#4672=LINE('',#23199,#5412);
#4673=LINE('',#23206,#5413);
#4674=LINE('',#23212,#5414);
#4675=LINE('',#23213,#5415);
#4676=LINE('',#23216,#5416);
#5398=VECTOR('',#18920,1.);
#5399=VECTOR('',#18925,1.);
#5400=VECTOR('',#18928,1.);
#5401=VECTOR('',#18933,1.);
#5402=VECTOR('',#18936,1.);
#5403=VECTOR('',#18941,1.);
#5404=VECTOR('',#18942,1.);
#5405=VECTOR('',#18943,1.);
#5406=VECTOR('',#18946,1.);
#5407=VECTOR('',#18947,1.);
#5408=VECTOR('',#18948,1.);
#5409=VECTOR('',#18951,1.);
#5410=VECTOR('',#18952,1.);
#5411=VECTOR('',#18953,1.);
#5412=VECTOR('',#18958,1.);
#5413=VECTOR('',#18969,1.);
#5414=VECTOR('',#18976,1.);
#5415=VECTOR('',#18977,1.);
#5416=VECTOR('',#18980,1.);
#6018=CIRCLE('',#15543,1.);
#6019=CIRCLE('',#15544,1.);
#6020=CIRCLE('',#15546,1.5);
#6021=CIRCLE('',#15547,1.5);
#6022=CIRCLE('',#15549,1.5);
#6023=CIRCLE('',#15550,1.5);
#6024=CIRCLE('',#15555,1.);
#6025=CIRCLE('',#15556,1.);
#6026=CIRCLE('',#15558,1.5);
#6027=CIRCLE('',#15559,1.5);
#6028=CIRCLE('',#15561,1.5);
#6029=CIRCLE('',#15562,1.);
#6030=CIRCLE('',#15565,1.);
#6031=CIRCLE('',#15567,1.5);
#7015=VERTEX_POINT('',#23154);
#7016=VERTEX_POINT('',#23156);
#7017=VERTEX_POINT('',#23160);
#7018=VERTEX_POINT('',#23161);
#7019=VERTEX_POINT('',#23163);
#7020=VERTEX_POINT('',#23165);
#7021=VERTEX_POINT('',#23169);
#7022=VERTEX_POINT('',#23170);
#7023=VERTEX_POINT('',#23172);
#7024=VERTEX_POINT('',#23174);
#7025=VERTEX_POINT('',#23178);
#7026=VERTEX_POINT('',#23180);
#7027=VERTEX_POINT('',#23184);
#7028=VERTEX_POINT('',#23186);
#7029=VERTEX_POINT('',#23190);
#7030=VERTEX_POINT('',#23192);
#7031=VERTEX_POINT('',#23196);
#7032=VERTEX_POINT('',#23198);
#7033=VERTEX_POINT('',#23205);
#7034=VERTEX_POINT('',#23208);
#7035=VERTEX_POINT('',#23211);
#7036=VERTEX_POINT('',#23215);
#8373=EDGE_CURVE('',#7015,#7015,#6018,.T.);
#8374=EDGE_CURVE('',#7015,#7016,#4658,.T.);
#8375=EDGE_CURVE('',#7016,#7016,#6019,.T.);
#8376=EDGE_CURVE('',#7017,#7018,#4659,.T.);
#8377=EDGE_CURVE('',#7017,#7019,#6020,.T.);
#8378=EDGE_CURVE('',#7020,#7019,#4660,.T.);
#8379=EDGE_CURVE('',#7018,#7020,#6021,.T.);
#8380=EDGE_CURVE('',#7021,#7022,#4661,.T.);
#8381=EDGE_CURVE('',#7023,#7021,#6022,.T.);
#8382=EDGE_CURVE('',#7024,#7023,#4662,.T.);
#8383=EDGE_CURVE('',#7024,#7022,#6023,.T.);
#8384=EDGE_CURVE('',#7025,#7023,#4663,.T.);
#8385=EDGE_CURVE('',#7025,#7026,#4664,.T.);
#8386=EDGE_CURVE('',#7026,#7024,#4665,.T.);
#8387=EDGE_CURVE('',#7022,#7027,#4666,.T.);
#8388=EDGE_CURVE('',#7027,#7028,#4667,.T.);
#8389=EDGE_CURVE('',#7021,#7028,#4668,.T.);
#8390=EDGE_CURVE('',#7019,#7029,#4669,.T.);
#8391=EDGE_CURVE('',#7029,#7030,#4670,.T.);
#8392=EDGE_CURVE('',#7020,#7030,#4671,.T.);
#8393=EDGE_CURVE('',#7031,#7031,#6024,.T.);
#8394=EDGE_CURVE('',#7031,#7032,#4672,.T.);
#8395=EDGE_CURVE('',#7032,#7032,#6025,.T.);
#8396=EDGE_CURVE('',#7030,#7025,#6026,.T.);
#8397=EDGE_CURVE('',#7029,#7026,#6027,.T.);
#8398=EDGE_CURVE('',#7033,#7017,#4673,.T.);
#8399=EDGE_CURVE('',#7027,#7033,#6028,.T.);
#8400=EDGE_CURVE('',#7034,#7034,#6029,.T.);
#8401=EDGE_CURVE('',#7035,#7018,#4674,.T.);
#8402=EDGE_CURVE('',#7035,#7033,#4675,.T.);
#8403=EDGE_CURVE('',#7034,#7036,#4676,.T.);
#8404=EDGE_CURVE('',#7036,#7036,#6030,.T.);
#8405=EDGE_CURVE('',#7028,#7035,#6031,.T.);
#10876=ORIENTED_EDGE('',*,*,#8373,.F.);
#10877=ORIENTED_EDGE('',*,*,#8374,.T.);
#10878=ORIENTED_EDGE('',*,*,#8375,.F.);
#10879=ORIENTED_EDGE('',*,*,#8374,.F.);
#10880=ORIENTED_EDGE('',*,*,#8376,.F.);
#10881=ORIENTED_EDGE('',*,*,#8377,.T.);
#10882=ORIENTED_EDGE('',*,*,#8378,.F.);
#10883=ORIENTED_EDGE('',*,*,#8379,.F.);
#10884=ORIENTED_EDGE('',*,*,#8380,.F.);
#10885=ORIENTED_EDGE('',*,*,#8381,.F.);
#10886=ORIENTED_EDGE('',*,*,#8382,.F.);
#10887=ORIENTED_EDGE('',*,*,#8383,.T.);
#10888=ORIENTED_EDGE('',*,*,#8382,.T.);
#10889=ORIENTED_EDGE('',*,*,#8384,.F.);
#10890=ORIENTED_EDGE('',*,*,#8385,.T.);
#10891=ORIENTED_EDGE('',*,*,#8386,.T.);
#10892=ORIENTED_EDGE('',*,*,#8380,.T.);
#10893=ORIENTED_EDGE('',*,*,#8387,.T.);
#10894=ORIENTED_EDGE('',*,*,#8388,.T.);
#10895=ORIENTED_EDGE('',*,*,#8389,.F.);
#10896=ORIENTED_EDGE('',*,*,#8378,.T.);
#10897=ORIENTED_EDGE('',*,*,#8390,.T.);
#10898=ORIENTED_EDGE('',*,*,#8391,.T.);
#10899=ORIENTED_EDGE('',*,*,#8392,.F.);
#10900=ORIENTED_EDGE('',*,*,#8393,.F.);
#10901=ORIENTED_EDGE('',*,*,#8394,.T.);
#10902=ORIENTED_EDGE('',*,*,#8395,.F.);
#10903=ORIENTED_EDGE('',*,*,#8394,.F.);
#10904=ORIENTED_EDGE('',*,*,#8385,.F.);
#10905=ORIENTED_EDGE('',*,*,#8396,.F.);
#10906=ORIENTED_EDGE('',*,*,#8391,.F.);
#10907=ORIENTED_EDGE('',*,*,#8397,.T.);
#10908=ORIENTED_EDGE('',*,*,#8398,.F.);
#10909=ORIENTED_EDGE('',*,*,#8399,.F.);
#10910=ORIENTED_EDGE('',*,*,#8387,.F.);
#10911=ORIENTED_EDGE('',*,*,#8383,.F.);
#10912=ORIENTED_EDGE('',*,*,#8386,.F.);
#10913=ORIENTED_EDGE('',*,*,#8397,.F.);
#10914=ORIENTED_EDGE('',*,*,#8390,.F.);
#10915=ORIENTED_EDGE('',*,*,#8377,.F.);
#10916=ORIENTED_EDGE('',*,*,#8373,.T.);
#10917=ORIENTED_EDGE('',*,*,#8393,.T.);
#10918=ORIENTED_EDGE('',*,*,#8400,.T.);
#10919=ORIENTED_EDGE('',*,*,#8376,.T.);
#10920=ORIENTED_EDGE('',*,*,#8401,.F.);
#10921=ORIENTED_EDGE('',*,*,#8402,.T.);
#10922=ORIENTED_EDGE('',*,*,#8398,.T.);
#10923=ORIENTED_EDGE('',*,*,#8400,.F.);
#10924=ORIENTED_EDGE('',*,*,#8403,.T.);
#10925=ORIENTED_EDGE('',*,*,#8404,.F.);
#10926=ORIENTED_EDGE('',*,*,#8403,.F.);
#10927=ORIENTED_EDGE('',*,*,#8388,.F.);
#10928=ORIENTED_EDGE('',*,*,#8399,.T.);
#10929=ORIENTED_EDGE('',*,*,#8402,.F.);
#10930=ORIENTED_EDGE('',*,*,#8405,.F.);
#10931=ORIENTED_EDGE('',*,*,#8389,.T.);
#10932=ORIENTED_EDGE('',*,*,#8405,.T.);
#10933=ORIENTED_EDGE('',*,*,#8401,.T.);
#10934=ORIENTED_EDGE('',*,*,#8379,.T.);
#10935=ORIENTED_EDGE('',*,*,#8392,.T.);
#10936=ORIENTED_EDGE('',*,*,#8396,.T.);
#10937=ORIENTED_EDGE('',*,*,#8384,.T.);
#10938=ORIENTED_EDGE('',*,*,#8381,.T.);
#10939=ORIENTED_EDGE('',*,*,#8375,.T.);
#10940=ORIENTED_EDGE('',*,*,#8395,.T.);
#10941=ORIENTED_EDGE('',*,*,#8404,.T.);
#12272=CYLINDRICAL_SURFACE('',#15542,1.);
#12273=CYLINDRICAL_SURFACE('',#15545,1.5);
#12274=CYLINDRICAL_SURFACE('',#15548,1.5);
#12275=CYLINDRICAL_SURFACE('',#15554,1.);
#12276=CYLINDRICAL_SURFACE('',#15557,1.5);
#12277=CYLINDRICAL_SURFACE('',#15564,1.);
#12278=CYLINDRICAL_SURFACE('',#15566,1.5);
#12903=ADVANCED_FACE('',(#2536),#12272,.F.);
#12904=ADVANCED_FACE('',(#2537),#12273,.T.);
#12905=ADVANCED_FACE('',(#2538),#12274,.T.);
#12906=ADVANCED_FACE('',(#2539),#1907,.T.);
#12907=ADVANCED_FACE('',(#2540),#1908,.T.);
#12908=ADVANCED_FACE('',(#2541),#1909,.T.);
#12909=ADVANCED_FACE('',(#2542),#12275,.F.);
#12910=ADVANCED_FACE('',(#2543),#12276,.T.);
#12911=ADVANCED_FACE('',(#2544,#1496,#1497,#1498),#1910,.F.);
#12912=ADVANCED_FACE('',(#2545),#1911,.T.);
#12913=ADVANCED_FACE('',(#2546),#12277,.F.);
#12914=ADVANCED_FACE('',(#2547),#12278,.T.);
#12915=ADVANCED_FACE('',(#2548,#1499,#1500,#1501),#1912,.T.);
#13310=CLOSED_SHELL('',(#12903,#12904,#12905,#12906,#12907,#12908,#12909,
#12910,#12911,#12912,#12913,#12914,#12915));
#15541=AXIS2_PLACEMENT_3D('',#23152,#18914,#18915);
#15542=AXIS2_PLACEMENT_3D('',#23153,#18916,#18917);
#15543=AXIS2_PLACEMENT_3D('',#23155,#18918,#18919);
#15544=AXIS2_PLACEMENT_3D('',#23158,#18921,#18922);
#15545=AXIS2_PLACEMENT_3D('',#23159,#18923,#18924);
#15546=AXIS2_PLACEMENT_3D('',#23164,#18926,#18927);
#15547=AXIS2_PLACEMENT_3D('',#23167,#18929,#18930);
#15548=AXIS2_PLACEMENT_3D('',#23168,#18931,#18932);
#15549=AXIS2_PLACEMENT_3D('',#23173,#18934,#18935);
#15550=AXIS2_PLACEMENT_3D('',#23176,#18937,#18938);
#15551=AXIS2_PLACEMENT_3D('',#23177,#18939,#18940);
#15552=AXIS2_PLACEMENT_3D('',#23183,#18944,#18945);
#15553=AXIS2_PLACEMENT_3D('',#23189,#18949,#18950);
#15554=AXIS2_PLACEMENT_3D('',#23195,#18954,#18955);
#15555=AXIS2_PLACEMENT_3D('',#23197,#18956,#18957);
#15556=AXIS2_PLACEMENT_3D('',#23200,#18959,#18960);
#15557=AXIS2_PLACEMENT_3D('',#23201,#18961,#18962);
#15558=AXIS2_PLACEMENT_3D('',#23202,#18963,#18964);
#15559=AXIS2_PLACEMENT_3D('',#23203,#18965,#18966);
#15560=AXIS2_PLACEMENT_3D('',#23204,#18967,#18968);
#15561=AXIS2_PLACEMENT_3D('',#23207,#18970,#18971);
#15562=AXIS2_PLACEMENT_3D('',#23209,#18972,#18973);
#15563=AXIS2_PLACEMENT_3D('',#23210,#18974,#18975);
#15564=AXIS2_PLACEMENT_3D('',#23214,#18978,#18979);
#15565=AXIS2_PLACEMENT_3D('',#23217,#18981,#18982);
#15566=AXIS2_PLACEMENT_3D('',#23218,#18983,#18984);
#15567=AXIS2_PLACEMENT_3D('',#23219,#18985,#18986);
#15568=AXIS2_PLACEMENT_3D('',#23220,#18987,#18988);
#18914=DIRECTION('axis',(0.,0.,1.));
#18915=DIRECTION('refdir',(1.,0.,0.));
#18916=DIRECTION('center_axis',(0.,1.,0.));
#18917=DIRECTION('ref_axis',(1.,0.,0.));
#18918=DIRECTION('center_axis',(0.,1.,0.));
#18919=DIRECTION('ref_axis',(1.,0.,0.));
#18920=DIRECTION('',(0.,1.,0.));
#18921=DIRECTION('center_axis',(0.,-1.,0.));
#18922=DIRECTION('ref_axis',(1.,0.,0.));
#18923=DIRECTION('center_axis',(0.,1.,0.));
#18924=DIRECTION('ref_axis',(1.,0.,0.));
#18925=DIRECTION('',(0.,1.,0.));
#18926=DIRECTION('center_axis',(0.,1.,0.));
#18927=DIRECTION('ref_axis',(1.,0.,0.));
#18928=DIRECTION('',(0.,-1.,0.));
#18929=DIRECTION('center_axis',(0.,1.,0.));
#18930=DIRECTION('ref_axis',(1.,0.,0.));
#18931=DIRECTION('center_axis',(0.,1.,0.));
#18932=DIRECTION('ref_axis',(1.,0.,0.));
#18933=DIRECTION('',(0.,-1.,0.));
#18934=DIRECTION('center_axis',(0.,1.,0.));
#18935=DIRECTION('ref_axis',(1.,0.,0.));
#18936=DIRECTION('',(0.,1.,0.));
#18937=DIRECTION('center_axis',(0.,1.,0.));
#18938=DIRECTION('ref_axis',(1.,0.,0.));
#18939=DIRECTION('center_axis',(0.25,0.,-0.968245836551854));
#18940=DIRECTION('ref_axis',(-0.968245836551854,0.,-0.25));
#18941=DIRECTION('',(-0.968245836551854,0.,-0.25));
#18942=DIRECTION('',(0.,-1.,0.));
#18943=DIRECTION('',(-0.968245836551854,0.,-0.25));
#18944=DIRECTION('center_axis',(0.25,0.,-0.968245836551854));
#18945=DIRECTION('ref_axis',(-0.968245836551854,0.,-0.25));
#18946=DIRECTION('',(-0.968245836551854,0.,-0.25));
#18947=DIRECTION('',(0.,1.,0.));
#18948=DIRECTION('',(-0.968245836551854,0.,-0.25));
#18949=DIRECTION('center_axis',(-0.25,0.,0.968245836551854));
#18950=DIRECTION('ref_axis',(0.968245836551854,0.,0.25));
#18951=DIRECTION('',(0.968245836551854,0.,0.25));
#18952=DIRECTION('',(0.,1.,0.));
#18953=DIRECTION('',(0.968245836551854,0.,0.25));
#18954=DIRECTION('center_axis',(0.,1.,0.));
#18955=DIRECTION('ref_axis',(1.,0.,0.));
#18956=DIRECTION('center_axis',(0.,1.,0.));
#18957=DIRECTION('ref_axis',(1.,0.,0.));
#18958=DIRECTION('',(0.,1.,0.));
#18959=DIRECTION('center_axis',(0.,-1.,0.));
#18960=DIRECTION('ref_axis',(1.,0.,0.));
#18961=DIRECTION('center_axis',(0.,1.,0.));
#18962=DIRECTION('ref_axis',(1.,0.,0.));
#18963=DIRECTION('center_axis',(0.,1.,0.));
#18964=DIRECTION('ref_axis',(1.,0.,0.));
#18965=DIRECTION('center_axis',(0.,1.,0.));
#18966=DIRECTION('ref_axis',(1.,0.,0.));
#18967=DIRECTION('center_axis',(0.,1.,0.));
#18968=DIRECTION('ref_axis',(1.,0.,0.));
#18969=DIRECTION('',(0.968245836551854,0.,0.25));
#18970=DIRECTION('center_axis',(0.,1.,0.));
#18971=DIRECTION('ref_axis',(1.,0.,0.));
#18972=DIRECTION('center_axis',(0.,1.,0.));
#18973=DIRECTION('ref_axis',(1.,0.,0.));
#18974=DIRECTION('center_axis',(-0.25,0.,0.968245836551854));
#18975=DIRECTION('ref_axis',(0.968245836551854,0.,0.25));
#18976=DIRECTION('',(0.968245836551854,0.,0.25));
#18977=DIRECTION('',(0.,-1.,0.));
#18978=DIRECTION('center_axis',(0.,1.,0.));
#18979=DIRECTION('ref_axis',(1.,0.,0.));
#18980=DIRECTION('',(0.,1.,0.));
#18981=DIRECTION('center_axis',(0.,-1.,0.));
#18982=DIRECTION('ref_axis',(1.,0.,0.));
#18983=DIRECTION('center_axis',(0.,1.,0.));
#18984=DIRECTION('ref_axis',(-0.968245836551854,0.,-0.250000000000002));
#18985=DIRECTION('center_axis',(0.,1.,0.));
#18986=DIRECTION('ref_axis',(1.,0.,0.));
#18987=DIRECTION('center_axis',(0.,1.,0.));
#18988=DIRECTION('ref_axis',(0.,0.,1.));
#23152=CARTESIAN_POINT('',(0.,0.,0.));
#23153=CARTESIAN_POINT('Origin',(19.3649167310371,4.9,8.));
#23154=CARTESIAN_POINT('',(18.3649167310371,5.,8.));
#23155=CARTESIAN_POINT('Origin',(19.3649167310371,5.,8.));
#23156=CARTESIAN_POINT('',(18.3649167310371,6.,8.));
#23157=CARTESIAN_POINT('',(18.3649167310371,4.9,8.));
#23158=CARTESIAN_POINT('Origin',(19.3649167310371,6.,8.));
#23159=CARTESIAN_POINT('Origin',(19.3649167310371,5.,8.));
#23160=CARTESIAN_POINT('',(18.1934954781404,5.,8.93689500386222));
#23161=CARTESIAN_POINT('',(18.1934954781404,6.,8.93689500386223));
#23162=CARTESIAN_POINT('',(18.1934954781404,5.,8.93689500386223));
#23163=CARTESIAN_POINT('',(19.9363379839338,5.,9.38689500386222));
#23164=CARTESIAN_POINT('Origin',(19.3649167310371,5.,8.));
#23165=CARTESIAN_POINT('',(19.9363379839338,6.,9.38689500386223));
#23166=CARTESIAN_POINT('',(19.9363379839338,5.,9.38689500386223));
#23167=CARTESIAN_POINT('Origin',(19.3649167310371,6.,8.));
#23168=CARTESIAN_POINT('Origin',(19.3649167310371,5.,8.));
#23169=CARTESIAN_POINT('',(18.7934954781404,6.,6.61310499613778));
#23170=CARTESIAN_POINT('',(18.7934954781404,5.,6.61310499613778));
#23171=CARTESIAN_POINT('',(18.7934954781404,5.,6.61310499613778));
#23172=CARTESIAN_POINT('',(20.5363379839338,6.,7.06310499613778));
#23173=CARTESIAN_POINT('Origin',(19.3649167310371,6.,8.));
#23174=CARTESIAN_POINT('',(20.5363379839338,5.,7.06310499613778));
#23175=CARTESIAN_POINT('',(20.5363379839338,5.,7.06310499613778));
#23176=CARTESIAN_POINT('Origin',(19.3649167310371,5.,8.));
#23177=CARTESIAN_POINT('Origin',(39.0298334620742,5.,11.8381049961378));
#23178=CARTESIAN_POINT('',(38.1584122091775,6.,11.6131049961378));
#23179=CARTESIAN_POINT('',(39.0298334620742,6.,11.8381049961378));
#23180=CARTESIAN_POINT('',(38.1584122091775,5.,11.6131049961378));
#23181=CARTESIAN_POINT('',(38.1584122091775,5.,11.6131049961378));
#23182=CARTESIAN_POINT('',(39.0298334620742,5.,11.8381049961378));
#23183=CARTESIAN_POINT('Origin',(39.0298334620742,5.,11.8381049961378));
#23184=CARTESIAN_POINT('',(1.17142125289667,5.,2.06310499613778));
#23185=CARTESIAN_POINT('',(39.0298334620742,5.,11.8381049961378));
#23186=CARTESIAN_POINT('',(1.17142125289667,6.,2.06310499613778));
#23187=CARTESIAN_POINT('',(1.17142125289667,5.,2.06310499613778));
#23188=CARTESIAN_POINT('',(39.0298334620742,6.,11.8381049961378));
#23189=CARTESIAN_POINT('Origin',(-0.3,5.,4.16189500386223));
#23190=CARTESIAN_POINT('',(37.5584122091775,5.,13.9368950038622));
#23191=CARTESIAN_POINT('',(-0.3,5.,4.16189500386223));
#23192=CARTESIAN_POINT('',(37.5584122091775,6.,13.9368950038622));
#23193=CARTESIAN_POINT('',(37.5584122091775,5.,13.9368950038622));
#23194=CARTESIAN_POINT('',(-0.3,6.,4.16189500386223));
#23195=CARTESIAN_POINT('Origin',(38.7298334620742,4.9,13.));
#23196=CARTESIAN_POINT('',(37.7298334620742,5.,13.));
#23197=CARTESIAN_POINT('Origin',(38.7298334620742,5.,13.));
#23198=CARTESIAN_POINT('',(37.7298334620742,6.,13.));
#23199=CARTESIAN_POINT('',(37.7298334620742,4.9,13.));
#23200=CARTESIAN_POINT('Origin',(38.7298334620742,6.,13.));
#23201=CARTESIAN_POINT('Origin',(38.7298334620742,5.,13.));
#23202=CARTESIAN_POINT('Origin',(38.7298334620742,6.,13.));
#23203=CARTESIAN_POINT('Origin',(38.7298334620742,5.,13.));
#23204=CARTESIAN_POINT('Origin',(19.3649167310371,5.,8.));
#23205=CARTESIAN_POINT('',(0.571421252896668,5.,4.38689500386223));
#23206=CARTESIAN_POINT('',(-0.3,5.,4.16189500386223));
#23207=CARTESIAN_POINT('Origin',(0.,5.,3.));
#23208=CARTESIAN_POINT('',(-1.,5.,3.));
#23209=CARTESIAN_POINT('Origin',(0.,5.,3.));
#23210=CARTESIAN_POINT('Origin',(-0.3,5.,4.16189500386223));
#23211=CARTESIAN_POINT('',(0.571421252896668,6.,4.38689500386223));
#23212=CARTESIAN_POINT('',(-0.3,6.,4.16189500386223));
#23213=CARTESIAN_POINT('',(0.571421252896668,5.,4.38689500386223));
#23214=CARTESIAN_POINT('Origin',(0.,4.9,3.));
#23215=CARTESIAN_POINT('',(-1.,6.,3.));
#23216=CARTESIAN_POINT('',(-1.,4.9,3.));
#23217=CARTESIAN_POINT('Origin',(0.,6.,3.));
#23218=CARTESIAN_POINT('Origin',(0.,5.,3.));
#23219=CARTESIAN_POINT('Origin',(0.,6.,3.));
#23220=CARTESIAN_POINT('Origin',(19.3649167310371,6.,8.));
#24926=UNCERTAINTY_MEASURE_WITH_UNIT(LENGTH_MEASURE(0.001),#25101,
'DISTANCE_ACCURACY_VALUE',
'Maximum model space distance between geometric entities at asserted c
onnectivities');
#24979=UNCERTAINTY_MEASURE_WITH_UNIT(LENGTH_MEASURE(0.001),#25101,
'DISTANCE_ACCURACY_VALUE',
'Maximum model space distance between geometric entities at asserted c
onnectivities');
#25047=(
GEOMETRIC_REPRESENTATION_CONTEXT(3)
GLOBAL_UNCERTAINTY_ASSIGNED_CONTEXT((#24926))
GLOBAL_UNIT_ASSIGNED_CONTEXT((#25101,#25103,#25104))
REPRESENTATION_CONTEXT('','3D')
);
#25100=(
GEOMETRIC_REPRESENTATION_CONTEXT(3)
GLOBAL_UNCERTAINTY_ASSIGNED_CONTEXT((#24979))
GLOBAL_UNIT_ASSIGNED_CONTEXT((#25101,#25103,#25104))
REPRESENTATION_CONTEXT('','3D')
);
#25101=(
LENGTH_UNIT()
NAMED_UNIT(*)
SI_UNIT(.CENTI.,.METRE.)
);
#25103=(
NAMED_UNIT(*)
PLANE_ANGLE_UNIT()
SI_UNIT($,.RADIAN.)
);
#25104=(
NAMED_UNIT(*)
SI_UNIT($,.STERADIAN.)
SOLID_ANGLE_UNIT()
);
#25172=SHAPE_DEFINITION_REPRESENTATION(#25294,#25577);
#25294=PRODUCT_DEFINITION_SHAPE('',$,#25698);
#25577=SHAPE_REPRESENTATION('',(#15541),#25047);
#25630=PRODUCT_DEFINITION_CONTEXT('part definition',#25992,'design');
#25698=PRODUCT_DEFINITION('Rising arm (1)','Rising arm (1)',#25818,#25630);
#25818=PRODUCT_DEFINITION_FORMATION('',$,#26061);
#25992=APPLICATION_CONTEXT(
'Core Data for Automotive Mechanical Design Process');
#25993=PRODUCT_CONTEXT('part definition',#25992,'mechanical');
#26061=PRODUCT('Rising arm (1)','Rising arm (1)','Rising arm (1)',(#25993));
#26171=COLOUR_RGB('Light Blue',0.38,0.62,0.78);
#26172=FILL_AREA_STYLE_COLOUR('',#26171);
#26173=FILL_AREA_STYLE('',(#26172));
#26174=SURFACE_STYLE_FILL_AREA(#26173);
#26175=SURFACE_SIDE_STYLE('',(#26174));
#26176=SURFACE_STYLE_USAGE(.BOTH.,#26175);
#26177=PRESENTATION_STYLE_ASSIGNMENT((#26176));
ENDSEC;
END-ISO-10303-21;
